ISO-10303-21;
HEADER;
/* Generated by software containing ST-Developer
 * from STEP Tools, Inc. (www.steptools.com) 
 */

FILE_DESCRIPTION(
/* description */ ('', 'CAx-IF Rec.Pracs.---Representation and Presentation of Product Manufa
cturing Information (PMI)---4.0---2014-10-13'),
/* implementation_level */ '2;1');

FILE_NAME(
/* name */ 'Shaft Washer.step',
/* time_stamp */ '2026-10-28T23:00:48+01:00',
/* author */ (''),
/* organization */ (''),
/* preprocessor_version */ 'ST-DEVELOPER v20.2',
/* originating_system */ 'Autodesk Translation Framework v15.17.0.0',
/* authorisation */ '');

FILE_SCHEMA (('AP242_MANAGED_MODEL_BASED_3D_ENGINEERING_MIM_LF { 1 0 10303 442 2 1 4 }'));
ENDSEC;

DATA;
#10=MECHANICAL_DESIGN_GEOMETRIC_PRESENTATION_REPRESENTATION('',(#995),#61811);
#931=SHAPE_REPRESENTATION_RELATIONSHIP('SRR','None',#61991,#956);
#956=ADVANCED_BREP_SHAPE_REPRESENTATION('',(#1034),#61804);
#995=STYLED_ITEM('',(#62163),#1034);
#1034=MANIFOLD_SOLID_BREP('Body1',#33825);
#1393=CYLINDRICAL_SURFACE('',#36123,18.5);
#1394=CYLINDRICAL_SURFACE('',#36126,33.);
#2129=FACE_BOUND('',#7400,.T.);
#2130=FACE_BOUND('',#7402,.T.);
#3121=CIRCLE('',#36124,18.5);
#3122=CIRCLE('',#36125,18.5);
#3123=CIRCLE('',#36127,33.);
#3124=CIRCLE('',#36128,33.);
#5268=FACE_OUTER_BOUND('',#7397,.T.);
#5269=FACE_OUTER_BOUND('',#7398,.T.);
#5270=FACE_OUTER_BOUND('',#7399,.T.);
#5271=FACE_OUTER_BOUND('',#7401,.T.);
#7397=EDGE_LOOP('',(#26566,#26567,#26568,#26569));
#7398=EDGE_LOOP('',(#26570,#26571,#26572,#26573));
#7399=EDGE_LOOP('',(#26574));
#7400=EDGE_LOOP('',(#26575));
#7401=EDGE_LOOP('',(#26576));
#7402=EDGE_LOOP('',(#26577));
#9824=LINE('',#56377,#12371);
#9825=LINE('',#56383,#12372);
#12371=VECTOR('',#43670,18.5);
#12372=VECTOR('',#43677,33.);
#15107=VERTEX_POINT('',#56374);
#15108=VERTEX_POINT('',#56376);
#15109=VERTEX_POINT('',#56380);
#15110=VERTEX_POINT('',#56382);
#19185=EDGE_CURVE('',#15107,#15107,#3121,.T.);
#19186=EDGE_CURVE('',#15107,#15108,#9824,.T.);
#19187=EDGE_CURVE('',#15108,#15108,#3122,.T.);
#19188=EDGE_CURVE('',#15109,#15109,#3123,.T.);
#19189=EDGE_CURVE('',#15109,#15110,#9825,.T.);
#19190=EDGE_CURVE('',#15110,#15110,#3124,.T.);
#26566=ORIENTED_EDGE('',*,*,#19185,.F.);
#26567=ORIENTED_EDGE('',*,*,#19186,.T.);
#26568=ORIENTED_EDGE('',*,*,#19187,.F.);
#26569=ORIENTED_EDGE('',*,*,#19186,.F.);
#26570=ORIENTED_EDGE('',*,*,#19188,.T.);
#26571=ORIENTED_EDGE('',*,*,#19189,.T.);
#26572=ORIENTED_EDGE('',*,*,#19190,.F.);
#26573=ORIENTED_EDGE('',*,*,#19189,.F.);
#26574=ORIENTED_EDGE('',*,*,#19188,.F.);
#26575=ORIENTED_EDGE('',*,*,#19187,.T.);
#26576=ORIENTED_EDGE('',*,*,#19190,.T.);
#26577=ORIENTED_EDGE('',*,*,#19185,.T.);
#31655=PLANE('',#36129);
#31656=PLANE('',#36130);
#32949=ADVANCED_FACE('',(#5268),#1393,.F.);
#32950=ADVANCED_FACE('',(#5269),#1394,.T.);
#32951=ADVANCED_FACE('',(#5270,#2129),#31655,.F.);
#32952=ADVANCED_FACE('',(#5271,#2130),#31656,.T.);
#33825=CLOSED_SHELL('',(#32949,#32950,#32951,#32952));
#36122=AXIS2_PLACEMENT_3D('',#56372,#43664,#43665);
#36123=AXIS2_PLACEMENT_3D('',#56373,#43666,#43667);
#36124=AXIS2_PLACEMENT_3D('',#56375,#43668,#43669);
#36125=AXIS2_PLACEMENT_3D('',#56378,#43671,#43672);
#36126=AXIS2_PLACEMENT_3D('',#56379,#43673,#43674);
#36127=AXIS2_PLACEMENT_3D('',#56381,#43675,#43676);
#36128=AXIS2_PLACEMENT_3D('',#56384,#43678,#43679);
#36129=AXIS2_PLACEMENT_3D('',#56385,#43680,#43681);
#36130=AXIS2_PLACEMENT_3D('',#56386,#43682,#43683);
#43664=DIRECTION('axis',(0.,0.,1.));
#43665=DIRECTION('refdir',(1.,0.,0.));
#43666=DIRECTION('center_axis',(-5.00596043934461E-16,-1.,-1.12027918221652E-15));
#43667=DIRECTION('ref_axis',(-5.46077161851015E-15,1.12027918221652E-15,
-1.));
#43668=DIRECTION('center_axis',(-5.00596043934461E-16,-1.,-1.12027918221652E-15));
#43669=DIRECTION('ref_axis',(-5.46077161851015E-15,1.12027918221652E-15,
-1.));
#43670=DIRECTION('',(-5.00596043934461E-16,-1.,-1.12027918221652E-15));
#43671=DIRECTION('center_axis',(5.00596043934461E-16,1.,1.12027918221652E-15));
#43672=DIRECTION('ref_axis',(-5.46077161851015E-15,1.12027918221652E-15,
-1.));
#43673=DIRECTION('center_axis',(-5.00596043934461E-16,-1.,-1.12027918221652E-15));
#43674=DIRECTION('ref_axis',(-5.46077161851015E-15,1.12027918221652E-15,
-1.));
#43675=DIRECTION('center_axis',(5.00596043934461E-16,1.,1.12027918221652E-15));
#43676=DIRECTION('ref_axis',(-5.46077161851015E-15,1.12027918221652E-15,
-1.));
#43677=DIRECTION('',(5.00596043934461E-16,1.,1.12027918221652E-15));
#43678=DIRECTION('center_axis',(5.00596043934461E-16,1.,1.12027918221652E-15));
#43679=DIRECTION('ref_axis',(-5.46077161851015E-15,1.12027918221652E-15,
-1.));
#43680=DIRECTION('center_axis',(5.00596043934461E-16,1.,1.12027918221652E-15));
#43681=DIRECTION('ref_axis',(-1.,5.00596043934455E-16,5.46077161851015E-15));
#43682=DIRECTION('center_axis',(5.00596043934461E-16,1.,1.12027918221652E-15));
#43683=DIRECTION('ref_axis',(-1.,5.00596043934455E-16,5.46077161851015E-15));
#56372=CARTESIAN_POINT('',(0.,0.,0.));
#56373=CARTESIAN_POINT('Origin',(263.115917770968,-255.47200726879,445.000000551893));
#56374=CARTESIAN_POINT('',(263.115917770968,-255.47200726879,463.500000551893));
#56375=CARTESIAN_POINT('Origin',(263.115917770968,-255.47200726879,445.000000551893));
#56376=CARTESIAN_POINT('',(263.115917770968,-260.47200726879,463.500000551893));
#56377=CARTESIAN_POINT('',(263.115917770968,-255.47200726879,463.500000551893));
#56378=CARTESIAN_POINT('Origin',(263.115917770968,-260.47200726879,445.000000551893));
#56379=CARTESIAN_POINT('Origin',(263.115917770968,-255.47200726879,445.000000551893));
#56380=CARTESIAN_POINT('',(263.115917770968,-260.47200726879,478.000000551893));
#56381=CARTESIAN_POINT('Origin',(263.115917770968,-260.47200726879,445.000000551893));
#56382=CARTESIAN_POINT('',(263.115917770968,-255.47200726879,478.000000551893));
#56383=CARTESIAN_POINT('',(263.115917770968,-255.47200726879,478.000000551893));
#56384=CARTESIAN_POINT('Origin',(263.115917770968,-255.47200726879,445.000000551893));
#56385=CARTESIAN_POINT('Origin',(263.115917770968,-260.47200726879,445.000000551893));
#56386=CARTESIAN_POINT('Origin',(263.115917770968,-255.47200726879,445.000000551893));
#61773=UNCERTAINTY_MEASURE_WITH_UNIT(LENGTH_MEASURE(0.01),#61812,
'DISTANCE_ACCURACY_VALUE',
'Maximum model space distance between geometric entities at asserted c
onnectivities');
#61780=UNCERTAINTY_MEASURE_WITH_UNIT(LENGTH_MEASURE(0.01),#61812,
'DISTANCE_ACCURACY_VALUE',
'Maximum model space distance between geometric entities at asserted c
onnectivities');
#61804=(
GEOMETRIC_REPRESENTATION_CONTEXT(3)
GLOBAL_UNCERTAINTY_ASSIGNED_CONTEXT((#61773))
GLOBAL_UNIT_ASSIGNED_CONTEXT((#61812,#61814,#61815))
REPRESENTATION_CONTEXT('','3D')
);
#61811=(
GEOMETRIC_REPRESENTATION_CONTEXT(3)
GLOBAL_UNCERTAINTY_ASSIGNED_CONTEXT((#61780))
GLOBAL_UNIT_ASSIGNED_CONTEXT((#61812,#61814,#61815))
REPRESENTATION_CONTEXT('','3D')
);
#61812=(
LENGTH_UNIT()
NAMED_UNIT(*)
SI_UNIT(.MILLI.,.METRE.)
);
#61814=(
NAMED_UNIT(*)
PLANE_ANGLE_UNIT()
SI_UNIT($,.RADIAN.)
);
#61815=(
NAMED_UNIT(*)
SI_UNIT($,.STERADIAN.)
SOLID_ANGLE_UNIT()
);
#61839=SHAPE_DEFINITION_REPRESENTATION(#61885,#61991);
#61885=PRODUCT_DEFINITION_SHAPE('',$,#62022);
#61991=SHAPE_REPRESENTATION('',(#36122),#61804);
#61998=PRODUCT_DEFINITION_CONTEXT('part definition',#62090,'design');
#62022=PRODUCT_DEFINITION('Shaft Washer','Shaft Washer',#62052,#61998);
#62052=PRODUCT_DEFINITION_FORMATION('',$,#62115);
#62090=APPLICATION_CONTEXT('Managed model based 3d engineering');
#62091=PRODUCT_CONTEXT('part definition',#62090,'mechanical');
#62115=PRODUCT('Shaft Washer','Shaft Washer',$,(#62091));
#62157=COLOUR_RGB('Black',0.12,0.14,0.17);
#62158=FILL_AREA_STYLE_COLOUR('',#62157);
#62159=FILL_AREA_STYLE('',(#62158));
#62160=SURFACE_STYLE_FILL_AREA(#62159);
#62161=SURFACE_SIDE_STYLE('',(#62160));
#62162=SURFACE_STYLE_USAGE(.BOTH.,#62161);
#62163=PRESENTATION_STYLE_ASSIGNMENT((#62162));
ENDSEC;
END-ISO-10303-21;
